ISO-10303-21;
HEADER;
FILE_DESCRIPTION (('STEP AP214'),
    '1' );
FILE_NAME ('socket button head screw_iso_ISO 7380 - M3 x 8 - 8N.step',
    '2026-10-26T05:17:54',
    ( '' ),
    ( '' ),
    'SwSTEP 2.0',
    'SolidWorks 2026',
    '' );
FILE_SCHEMA (( 'AUTOMOTIVE_DESIGN' ));
ENDSEC;

DATA;
#25=PLANE ( 'NONE',  #12625 ) ;
#33=EDGE_LOOP ( 'NONE', ( #5496, #9068, #8693 ) ) ;
#38=CARTESIAN_POINT ( 'NONE',  ( 0.000000000000000000, -0.5773502691896255090, 1.000000000000000000 ) ) ;
#50=DIRECTION ( 'NONE',  ( 0.000000000000000000, 0.000000000000000000, -1.000000000000000000 ) ) ;
#58=VERTEX_POINT ( 'NONE', #1081 ) ;
#82=FACE_OUTER_BOUND ( 'NONE', #972, .T. ) ;
#95=ORIENTED_EDGE ( 'NONE', *, *, #10637, .F. ) ;
#97=EDGE_CURVE ( 'NONE', #1488, #5076, #12936, .T. ) ;
#100=SURFACE_SIDE_STYLE ('',( #3136 ) ) ;
#102=ORIENTED_EDGE ( 'NONE', *, *, #8081, .F. ) ;
#125=ADVANCED_FACE ( 'NONE', ( #2807 ), #25, .T. ) ;
#132=ORIENTED_EDGE ( 'NONE', *, *, #9753, .F. ) ;
#135=ORIENTED_EDGE ( 'NONE', *, *, #4811, .F. ) ;
#186=AXIS2_PLACEMENT_3D ( 'NONE', #1840, #9816, #9754 ) ;
#211=CARTESIAN_POINT ( 'NONE',  ( 1.040000000000000036, -1.154700538379251240, 1.014316938424154191E-17 ) ) ;
#215=FACE_OUTER_BOUND ( 'NONE', #2493, .T. ) ;
#228=( NAMED_UNIT ( * ) SI_UNIT ( $, .STERADIAN. ) SOLID_ANGLE_UNIT ( ) );
#246=ORIENTED_EDGE ( 'NONE', *, *, #10941, .F. ) ;
#249=VECTOR ( 'NONE', #11495, 1000.000000000000000 ) ;
#320=CONICAL_SURFACE ( 'NONE', #5556, 1732.050807568857181, 1.047197551196592746 ) ;
#322=EDGE_CURVE ( 'NONE', #7840, #11587, #9067, .T. ) ;
#324=( GEOMETRIC_REPRESENTATION_CONTEXT ( 3 ) GLOBAL_UNCERTAINTY_ASSIGNED_CONTEXT ( ( #7109 ) ) GLOBAL_UNIT_ASSIGNED_CONTEXT ( ( #5148, #12551, #626 ) ) REPRESENTATION_CONTEXT ( 'NONE', 'WORKASPACE' ) );
#333=CIRCLE ( 'NONE', #7661, 2.849999999999999201 ) ;
#350=AXIS2_PLACEMENT_3D ( 'NONE', #7687, #12398, #1471 ) ;
#392=ORIENTED_EDGE ( 'NONE', *, *, #8088, .T. ) ;
#420=FACE_OUTER_BOUND ( 'NONE', #4531, .T. ) ;
#464=EDGE_CURVE ( 'NONE', #9403, #7005, #12208, .T. ) ;
#468=DIRECTION ( 'NONE',  ( 1.000000000000000000, 0.000000000000000000, 0.000000000000000000 ) ) ;
#488=VERTEX_POINT ( 'NONE', #6898 ) ;
#505=CARTESIAN_POINT ( 'NONE',  ( 9.369499999999998607, 0.000000000000000000, 0.000000000000000000 ) ) ;
#530=AXIS2_PLACEMENT_3D ( 'NONE', #7357, #8344, #1205 ) ;
#540=AXIS2_PLACEMENT_3D ( 'NONE', #1275, #10104, #5264 ) ;
#545=CARTESIAN_POINT ( 'NONE',  ( 1.617350269189632428, 0.000000000000000000, 0.000000000000000000 ) ) ;
#562=FACE_OUTER_BOUND ( 'NONE', #1188, .T. ) ;
#571=VERTEX_POINT ( 'NONE', #2859 ) ;
#580=VECTOR ( 'NONE', #12744, 1000.000000000000000 ) ;
#595=DIRECTION ( 'NONE',  ( -0.000000000000000000, -1.000000000000000000, -0.000000000000000000 ) ) ;
#598=CARTESIAN_POINT ( 'NONE',  ( 0.000000000000000000, -0.5773502691896256200, -1.000000000000000000 ) ) ;
#613=LINE ( 'NONE', #545, #2256 ) ;
#620=PLANE ( 'NONE',  #2626 ) ;
#623=ORIENTED_EDGE ( 'NONE', *, *, #10337, .T. ) ;
#626=( NAMED_UNIT ( * ) SI_UNIT ( $, .STERADIAN. ) SOLID_ANGLE_UNIT ( ) );
#627=ORIENTED_EDGE ( 'NONE', *, *, #322, .T. ) ;
#632=EDGE_CURVE ( 'NONE', #11636, #4911, #11998, .T. ) ;
#638=ORIENTED_EDGE ( 'NONE', *, *, #97, .F. ) ;
#639=DIRECTION ( 'NONE',  ( -1.000000000000000000, -0.000000000000000000, -0.000000000000000000 ) ) ;
#678=EDGE_CURVE ( 'NONE', #12162, #3526, #8342, .T. ) ;
#686=DIRECTION ( 'NONE',  ( 0.000000000000000000, 0.000000000000000000, 1.000000000000000000 ) ) ;
#713=AXIS2_PLACEMENT_3D ( 'NONE', #1399, #12460, #4544 ) ;
#771=ORIENTED_EDGE ( 'NONE', *, *, #10941, .T. ) ;
#773=ORIENTED_EDGE ( 'NONE', *, *, #1233, .T. ) ;
#779=ORIENTED_EDGE ( 'NONE', *, *, #2404, .T. ) ;
#818=CARTESIAN_POINT ( 'NONE',  ( 9.650000000000000355, 0.000000000000000000, 0.000000000000000000 ) ) ;
#824=ADVANCED_FACE ( 'NONE', ( #3571 ), #6132, .F. ) ;
#845=DIRECTION ( 'NONE',  ( 0.000000000000000000, 0.000000000000000000, 1.000000000000000000 ) ) ;
#854=CARTESIAN_POINT ( 'NONE',  ( -998.3826497308103853, 0.000000000000000000, 0.000000000000000000 ) ) ;
#859=CARTESIAN_POINT ( 'NONE',  ( 1.040000000000000036, -0.5773502691896256200, -1.000000000000000000 ) ) ;
#860=LINE ( 'NONE', #11926, #9943 ) ;
#865=VERTEX_POINT ( 'NONE', #12592 ) ;
#926=CARTESIAN_POINT ( 'NONE',  ( -998.3826497308103853, 0.000000000000000000, 0.000000000000000000 ) ) ;
#945=CARTESIAN_POINT ( 'NONE',  ( 1.269999999999999796, 3.490243377569955568E-16, -2.849999999999999201 ) ) ;
#960=FILL_AREA_STYLE_COLOUR ( '', #10521 ) ;
#972=EDGE_LOOP ( 'NONE', ( #6350, #4719, #5970 ) ) ;
#976=EDGE_CURVE ( 'NONE', #11967, #1106, #7871, .T. ) ;
#983=DIRECTION ( 'NONE',  ( -0.000000000000000000, 0.000000000000000000, 1.000000000000000000 ) ) ;
#1023=EDGE_CURVE ( 'NONE', #9939, #1488, #2969, .T. ) ;
#1044=CIRCLE ( 'NONE', #2106, 1.599999999999998757 ) ;
#1049=EDGE_CURVE ( 'NONE', #58, #8179, #6691, .T. ) ;
#1051=AXIS2_PLACEMENT_3D ( 'NONE', #10287, #5252, #6234 ) ;
#1064=CARTESIAN_POINT ( 'NONE',  ( 1.040000000000000036, -0.8660254037844385966, 0.4999999999999997780 ) ) ;
#1076=ORIENTED_EDGE ( 'NONE', *, *, #10227, .T. ) ;
#1081=CARTESIAN_POINT ( 'NONE',  ( 1.040000000000000036, -1.154700538379251240, 1.014316938424154191E-17 ) ) ;
#1091=ORIENTED_EDGE ( 'NONE', *, *, #8626, .F. ) ;
#1098=CARTESIAN_POINT ( 'NONE',  ( 1.040000000000000036, 0.000000000000000000, 2.000000000000000000 ) ) ;
#1106=VERTEX_POINT ( 'NONE', #10081 ) ;
#1119=EDGE_LOOP ( 'NONE', ( #1583, #11044, #4776, #9799 ) ) ;
#1133=CARTESIAN_POINT ( 'NONE',  ( 1.649999999999999023, 0.000000000000000000, 0.000000000000000000 ) ) ;
#1142=DIRECTION ( 'NONE',  ( -0.000000000000000000, 0.000000000000000000, 1.000000000000000000 ) ) ;
#1188=EDGE_LOOP ( 'NONE', ( #638, #12953, #4691 ) ) ;
#1205=DIRECTION ( 'NONE',  ( -0.000000000000000000, 0.000000000000000000, 1.000000000000000000 ) ) ;
#1207=DIRECTION ( 'NONE',  ( 0.000000000000000000, 0.4999999999999998890, 0.8660254037844387076 ) ) ;
#1233=EDGE_CURVE ( 'NONE', #11967, #3765, #2195, .T. ) ;
#1275=CARTESIAN_POINT ( 'NONE',  ( 0.000000000000000000, 0.000000000000000000, 0.000000000000000000 ) ) ;
#1295=DIRECTION ( 'NONE',  ( -0.000000000000000000, 0.5000000000000003331, 0.8660254037844384856 ) ) ;
#1355=DIRECTION ( 'NONE',  ( 0.000000000000000000, 0.000000000000000000, -1.000000000000000000 ) ) ;
#1374=ADVANCED_BREP_SHAPE_REPRESENTATION ( '', ( #3541, #5704 ), #11138 ) ;
#1375=CARTESIAN_POINT ( 'NONE',  ( 1.040000000000000036, 0.8660254037844393737, 0.5000000000000007772 ) ) ;
#1391=DIRECTION ( 'NONE',  ( -0.000000000000000000, 0.4999999999999998890, -0.8660254037844387076 ) ) ;
#1399=CARTESIAN_POINT ( 'NONE',  ( 1.749999999999999112, 0.000000000000000000, 0.000000000000000000 ) ) ;
#1435=ADVANCED_FACE ( 'NONE', ( #9923 ), #7967, .T. ) ;
#1451=PRODUCT ( 'socket button head screw_iso_ISO 7380 - M3 x 8 - 8N', 'socket button head screw_iso_ISO 7380 - M3 x 8 - 8N', '', ( #10334 ) ) ;
#1471=DIRECTION ( 'NONE',  ( 0.000000000000000000, 0.000000000000000000, 1.000000000000000000 ) ) ;
#1488=VERTEX_POINT ( 'NONE', #11030 ) ;
#1490=LINE ( 'NONE', #7512, #249 ) ;
#1528=VECTOR ( 'NONE', #12804, 1000.000000000000000 ) ;
#1533=CARTESIAN_POINT ( 'NONE',  ( 9.369499999999998607, 1.836970198721030181E-16, -1.500000000000000444 ) ) ;
#1546=EDGE_LOOP ( 'NONE', ( #6390, #5719, #779, #12274, #2661 ) ) ;
#1561=CIRCLE ( 'NONE', #8871, 1.000000000000000000 ) ;
#1565=ADVANCED_FACE ( 'NONE', ( #420 ), #5276, .T. ) ;
#1583=ORIENTED_EDGE ( 'NONE', *, *, #4614, .T. ) ;
#1588=DIRECTION ( 'NONE',  ( 0.000000000000000000, -1.224646799147353207E-16, 1.000000000000000000 ) ) ;
#1590=APPLICATION_CONTEXT ( 'automotive_design' ) ;
#1676=DIRECTION ( 'NONE',  ( 0.000000000000000000, 0.000000000000000000, 1.000000000000000000 ) ) ;
#1701=VERTEX_POINT ( 'NONE', #2472 ) ;
#1749=DIRECTION ( 'NONE',  ( -1.000000000000000000, -0.000000000000000000, -0.000000000000000000 ) ) ;
#1751=LINE ( 'NONE', #9733, #1528 ) ;
#1787=ADVANCED_FACE ( 'NONE', ( #9594 ), #620, .T. ) ;
#1803=EDGE_CURVE ( 'NONE', #4911, #5204, #10636, .T. ) ;
#1814=AXIS2_PLACEMENT_3D ( 'NONE', #4355, #4548, #12595 ) ;
#1840=CARTESIAN_POINT ( 'NONE',  ( 1.269999999999999796, 0.000000000000000000, 0.000000000000000000 ) ) ;
#1916=DIRECTION ( 'NONE',  ( -1.000000000000000000, -0.000000000000000000, -0.000000000000000000 ) ) ;
#1938=DIRECTION ( 'NONE',  ( -1.000000000000000000, -0.000000000000000000, -0.000000000000000000 ) ) ;
#1970=ORIENTED_EDGE ( 'NONE', *, *, #9131, .F. ) ;
#1982=CARTESIAN_POINT ( 'NONE',  ( 1.040000000000000036, -0.5773502691896255090, 1.000000000000000000 ) ) ;
#1994=AXIS2_PLACEMENT_3D ( 'NONE', #7112, #2938, #9003 ) ;
#1996=AXIS2_PLACEMENT_3D ( 'NONE', #11776, #12764, #12891 ) ;
#2002=ADVANCED_FACE ( 'NONE', ( #5130 ), #4352, .F. ) ;
#2034=ORIENTED_EDGE ( 'NONE', *, *, #10337, .F. ) ;
#2069=FACE_OUTER_BOUND ( 'NONE', #3154, .T. ) ;
#2076=AXIS2_PLACEMENT_3D ( 'NONE', #8907, #3819, #6686 ) ;
#2090=ORIENTED_EDGE ( 'NONE', *, *, #9698, .T. ) ;
#2104=VECTOR ( 'NONE', #11623, 1000.000000000000000 ) ;
#2106=AXIS2_PLACEMENT_3D ( 'NONE', #1133, #12199, #12265 ) ;
#2130=CARTESIAN_POINT ( 'NONE',  ( 0.000000000000000000, 0.5773502691896262862, 1.000000000000000000 ) ) ;
#2136=FACE_BOUND ( 'NONE', #12116, .T. ) ;
#2154=ORIENTED_EDGE ( 'NONE', *, *, #12163, .T. ) ;
#2156=ORIENTED_EDGE ( 'NONE', *, *, #5971, .T. ) ;
#2159=ORIENTED_EDGE ( 'NONE', *, *, #7690, .F. ) ;
#2195=CIRCLE ( 'NONE', #3245, 1.500000000000000222 ) ;
#2202=DIRECTION ( 'NONE',  ( 0.000000000000000000, 0.000000000000000000, 1.000000000000000000 ) ) ;
#2228=DIRECTION ( 'NONE',  ( -1.000000000000000000, 0.000000000000000000, -0.000000000000000000 ) ) ;
#2236=VECTOR ( 'NONE', #595, 1000.000000000000000 ) ;
#2247=CARTESIAN_POINT ( 'NONE',  ( 1.269999999999999796, 0.000000000000000000, 2.849999999999999201 ) ) ;
#2254=CARTESIAN_POINT ( 'NONE',  ( 1.649999999999999023, 1.959434878635763258E-16, -1.599999999999998757 ) ) ;
#2256=VECTOR ( 'NONE', #11478, 1000.000000000000114 ) ;
#2275=ORIENTED_EDGE ( 'NONE', *, *, #6757, .T. ) ;
#2285=ORIENTED_EDGE ( 'NONE', *, *, #11434, .T. ) ;
#2302=AXIS2_PLACEMENT_3D ( 'NONE', #9764, #8659, #7932 ) ;
#2337=CARTESIAN_POINT ( 'NONE',  ( 1.649999999999999911, 0.000000000000000000, 2.849999999999999201 ) ) ;
#2341=DIRECTION ( 'NONE',  ( -1.000000000000000000, 0.000000000000000000, 0.000000000000000000 ) ) ;
#2353=ADVANCED_FACE ( 'NONE', ( #3894 ), #320, .F. ) ;
#2381=CARTESIAN_POINT ( 'NONE',  ( 1.269999999999999796, 0.000000000000000000, 0.000000000000000000 ) ) ;
#2393=LINE ( 'NONE', #211, #2946 ) ;
#2404=EDGE_CURVE ( 'NONE', #10269, #7344, #860, .T. ) ;
#2434=DIRECTION ( 'NONE',  ( -0.000000000000000000, 0.5000000000000003331, 0.8660254037844384856 ) ) ;
#2440=CIRCLE ( 'NONE', #4313, 1.219500000000000028 ) ;
#2472=CARTESIAN_POINT ( 'NONE',  ( 0.000000000000000000, -1.154700538379251240, 1.014316938424154191E-17 ) ) ;
#2485=VECTOR ( 'NONE', #6651, 1000.000000000000000 ) ;
#2493=EDGE_LOOP ( 'NONE', ( #12356, #6274 ) ) ;
#2502=CONICAL_SURFACE ( 'NONE', #9807, 1732.050807568857181, 1.047197551196592746 ) ;
#2507=VERTEX_POINT ( 'NONE', #2254 ) ;
#2527=DIRECTION ( 'NONE',  ( -1.000000000000000000, -0.000000000000000000, -0.000000000000000000 ) ) ;
#2559=EDGE_LOOP ( 'NONE', ( #102, #5637, #7763, #11235 ) ) ;
#2567=EDGE_CURVE ( 'NONE', #12299, #11967, #8135, .T. ) ;
#2568=DIRECTION ( 'NONE',  ( -1.000000000000000000, -0.000000000000000000, -0.000000000000000000 ) ) ;
#2607=VECTOR ( 'NONE', #5725, 1000.000000000000000 ) ;
#2615=VECTOR ( 'NONE', #3758, 1000.000000000000000 ) ;
#2626=AXIS2_PLACEMENT_3D ( 'NONE', #11682, #4497, #10508 ) ;
#2651=DIRECTION ( 'NONE',  ( 0.000000000000000000, 0.000000000000000000, 1.000000000000000000 ) ) ;
#2661=ORIENTED_EDGE ( 'NONE', *, *, #10729, .F. ) ;
#2662=AXIS2_PLACEMENT_3D ( 'NONE', #818, #1938, #3975 ) ;
#2667=CARTESIAN_POINT ( 'NONE',  ( 1.040000000000000036, 1.154700538379252350, 7.017607234860990640E-28 ) ) ;
#2675=FACE_OUTER_BOUND ( 'NONE', #12632, .T. ) ;
#2676=CARTESIAN_POINT ( 'NONE',  ( 1.040000000000000036, 0.000000000000000000, 2.000000000000000000 ) ) ;
#2679=ORIENTED_EDGE ( 'NONE', *, *, #10729, .T. ) ;
#2708=LINE ( 'NONE', #12109, #3815 ) ;
#2717=AXIS2_PLACEMENT_3D ( 'NONE', #11906, #9944, #12824 ) ;
#2734=CIRCLE ( 'NONE', #2935, 1.000000000000000000 ) ;
#2738=DIRECTION ( 'NONE',  ( -1.000000000000000000, 0.000000000000000000, 0.000000000000000000 ) ) ;
#2752=ORIENTED_EDGE ( 'NONE', *, *, #2404, .F. ) ;
#2768=ORIENTED_EDGE ( 'NONE', *, *, #12870, .T. ) ;
#2807=FACE_OUTER_BOUND ( 'NONE', #33, .T. ) ;
#2859=CARTESIAN_POINT ( 'NONE',  ( 1.040000000000000036, 0.000000000000000000, -1.000000000000000000 ) ) ;
#2860=STYLED_ITEM('',(#13009),#3541);
#2916=EDGE_CURVE ( 'NONE', #10444, #3526, #1751, .T. ) ;
#2935=AXIS2_PLACEMENT_3D ( 'NONE', #6372, #4293, #8475 ) ;
#2938=DIRECTION ( 'NONE',  ( -1.000000000000000000, -0.000000000000000000, -0.000000000000000000 ) ) ;
#2946=VECTOR ( 'NONE', #6500, 1000.000000000000000 ) ;
#2969=LINE ( 'NONE', #5778, #3868 ) ;
#2973=CARTESIAN_POINT ( 'NONE',  ( 4.336808689942017736E-16, 0.000000000000000000, 0.000000000000000000 ) ) ;
#2975=ORIENTED_EDGE ( 'NONE', *, *, #8127, .T. ) ;
#3037=UNCERTAINTY_MEASURE_WITH_UNIT (LENGTH_MEASURE( 1.000000000000000082E-05 ), #7177, 'distance_accuracy_value', 'NONE');
#3045=DIRECTION ( 'NONE',  ( 0.000000000000000000, 0.000000000000000000, 1.000000000000000000 ) ) ;
#3069=( LENGTH_UNIT ( ) NAMED_UNIT ( * ) SI_UNIT ( .MILLI., .METRE. ) );
#3136=SURFACE_STYLE_FILL_AREA ( #12943 ) ;
#3142=DIRECTION ( 'NONE',  ( 0.000000000000000000, 0.000000000000000000, 1.000000000000000000 ) ) ;
#3154=EDGE_LOOP ( 'NONE', ( #8578, #623, #2679, #7603, #5681 ) ) ;
#3161=FACE_OUTER_BOUND ( 'NONE', #9940, .T. ) ;
#3165=EDGE_CURVE ( 'NONE', #9939, #11636, #9935, .T. ) ;
#3174=VERTEX_POINT ( 'NONE', #10809 ) ;
#3245=AXIS2_PLACEMENT_3D ( 'NONE', #505, #639, #6531 ) ;
#3253=FACE_OUTER_BOUND ( 'NONE', #12430, .T. ) ;
#3273=ORIENTED_EDGE ( 'NONE', *, *, #464, .F. ) ;
#3277=DIRECTION ( 'NONE',  ( 0.000000000000000000, 1.000000000000000000, 0.000000000000000000 ) ) ;
#3285=EDGE_CURVE ( 'NONE', #9018, #9939, #11443, .T. ) ;
#3330=DIRECTION ( 'NONE',  ( -1.000000000000000000, -0.000000000000000000, -0.000000000000000000 ) ) ;
#3332=ORIENTED_EDGE ( 'NONE', *, *, #4614, .F. ) ;
#3369=DIRECTION ( 'NONE',  ( -1.000000000000000000, -0.000000000000000000, -0.000000000000000000 ) ) ;
#3371=LINE ( 'NONE', #598, #9575 ) ;
#3389=DIRECTION ( 'NONE',  ( 0.000000000000000000, 0.000000000000000000, 1.000000000000000000 ) ) ;
#3396=CARTESIAN_POINT ( 'NONE',  ( 0.000000000000000000, 0.5773502691896262862, 1.000000000000000000 ) ) ;
#3397=EDGE_LOOP ( 'NONE', ( #10965, #5431, #5265, #7983, #392 ) ) ;
#3429=DIRECTION ( 'NONE',  ( 0.000000000000000000, 0.000000000000000000, 1.000000000000000000 ) ) ;
#3450=AXIS2_PLACEMENT_3D ( 'NONE', #6445, #12403, #1676 ) ;
#3460=CIRCLE ( 'NONE', #10117, 1.599999999999998757 ) ;
#3465=CARTESIAN_POINT ( 'NONE',  ( 1.040000000000000036, 0.000000000000000000, 2.000000000000000000 ) ) ;
#3479=VERTEX_POINT ( 'NONE', #7312 ) ;
#3487=CONICAL_SURFACE ( 'NONE', #5138, 1.219500000000000028, 0.7853981633974463916 ) ;
#3494=EDGE_CURVE ( 'NONE', #12299, #10459, #2440, .T. ) ;
#3526=VERTEX_POINT ( 'NONE', #3396 ) ;
#3541=MANIFOLD_SOLID_BREP ( 'Hex', #5303 ) ;
#3569=ADVANCED_FACE ( 'NONE', ( #6582 ), #3487, .T. ) ;
#3571=FACE_OUTER_BOUND ( 'NONE', #2559, .T. ) ;
#3576=FACE_OUTER_BOUND ( 'NONE', #9791, .T. ) ;
#3596=DIRECTION ( 'NONE',  ( -1.000000000000000000, 0.000000000000000000, 0.000000000000000000 ) ) ;
#3623=ORIENTED_EDGE ( 'NONE', *, *, #3285, .T. ) ;
#3642=CARTESIAN_POINT ( 'NONE',  ( 1.040000000000000036, 0.8660254037844391517, -0.5000000000000006661 ) ) ;
#3646=CARTESIAN_POINT ( 'NONE',  ( 1.040000000000000036, 1.154700538379252350, 7.017607234860990640E-28 ) ) ;
#3654=CARTESIAN_POINT ( 'NONE',  ( 9.650000000000000355, 0.000000000000000000, 0.000000000000000000 ) ) ;
#3659=ORIENTED_EDGE ( 'NONE', *, *, #3165, .T. ) ;
#3662=DIRECTION ( 'NONE',  ( 0.000000000000000000, 0.000000000000000000, 1.000000000000000000 ) ) ;
#3721=PLANE ( 'NONE',  #7706 ) ;
#3724=EDGE_CURVE ( 'NONE', #7344, #11587, #3972, .T. ) ;
#3758=DIRECTION ( 'NONE',  ( -1.000000000000000000, 0.000000000000000000, 0.000000000000000000 ) ) ;
#3765=VERTEX_POINT ( 'NONE', #9722 ) ;
#3809=ORIENTED_EDGE ( 'NONE', *, *, #9698, .F. ) ;
#3815=VECTOR ( 'NONE', #10074, 1000.000000000000000 ) ;
#3819=DIRECTION ( 'NONE',  ( 0.000000000000000000, -0.8660254037844384856, 0.5000000000000003331 ) ) ;
#3823=DIRECTION ( 'NONE',  ( -1.000000000000000000, -0.000000000000000000, -0.000000000000000000 ) ) ;
#3848=FACE_OUTER_BOUND ( 'NONE', #8032, .T. ) ;
#3853=ADVANCED_FACE ( 'NONE', ( #2069 ), #6047, .T. ) ;
#3868=VECTOR ( 'NONE', #9831, 1000.000000000000000 ) ;
#3878=ADVANCED_FACE ( 'NONE', ( #3253 ), #6110, .T. ) ;
#3894=FACE_OUTER_BOUND ( 'NONE', #3397, .T. ) ;
#3908=DIRECTION ( 'NONE',  ( -1.000000000000000000, 0.000000000000000000, 0.000000000000000000 ) ) ;
#3919=DIRECTION ( 'NONE',  ( 0.000000000000000000, 0.000000000000000000, 1.000000000000000000 ) ) ;
#3930=ADVANCED_FACE ( 'NONE', ( #6374 ), #7457, .T. ) ;
#3972=LINE ( 'NONE', #7823, #7240 ) ;
#3975=DIRECTION ( 'NONE',  ( 0.000000000000000000, 0.000000000000000000, 1.000000000000000000 ) ) ;
#3987=SURFACE_STYLE_USAGE ( .BOTH. , #100 ) ;
#4003=ORIENTED_EDGE ( 'NONE', *, *, #2916, .T. ) ;
#4035=ORIENTED_EDGE ( 'NONE', *, *, #3494, .F. ) ;
#4060=ORIENTED_EDGE ( 'NONE', *, *, #9131, .T. ) ;
#4062=EDGE_CURVE ( 'NONE', #11890, #1701, #8334, .T. ) ;
#4072=CARTESIAN_POINT ( 'NONE',  ( 0.000000000000000000, 1.154700538379252350, 7.017607234860990640E-28 ) ) ;
#4084=EDGE_LOOP ( 'NONE', ( #2156, #12544, #8259, #12865, #7300 ) ) ;
#4091=EDGE_CURVE ( 'NONE', #10444, #9939, #4535, .T. ) ;
#4101=CARTESIAN_POINT ( 'NONE',  ( 1.040000000000000036, -1.154700538379251240, 1.014316938424154191E-17 ) ) ;
#4123=EDGE_CURVE ( 'NONE', #4591, #9403, #333, .T. ) ;
#4174=APPLICATION_CONTEXT ( 'automotive_design' ) ;
#4182=CYLINDRICAL_SURFACE ( 'NONE', #12783, 1.499999999999998668 ) ;
#4185=DIRECTION ( 'NONE',  ( 0.000000000000000000, 0.000000000000000000, -1.000000000000000000 ) ) ;
#4189=ORIENTED_EDGE ( 'NONE', *, *, #12070, .T. ) ;
#4198=AXIS2_PLACEMENT_3D ( 'NONE', #11146, #3908, #2202 ) ;
#4293=DIRECTION ( 'NONE',  ( -1.000000000000000000, -0.000000000000000000, -0.000000000000000000 ) ) ;
#4313=AXIS2_PLACEMENT_3D ( 'NONE', #8168, #10188, #8365 ) ;
#4338=CARTESIAN_POINT ( 'NONE',  ( 9.650000000000000355, 1.493456771560197319E-16, -1.219500000000000028 ) ) ;
#4352=PLANE ( 'NONE',  #530 ) ;
#4355=CARTESIAN_POINT ( 'NONE',  ( 9.650000000000000355, 0.000000000000000000, 0.000000000000000000 ) ) ;
#4359=PLANE ( 'NONE',  #9347 ) ;
#4366=AXIS2_PLACEMENT_3D ( 'NONE', #10360, #10230, #9048 ) ;
#4368=CARTESIAN_POINT ( 'NONE',  ( 1.040000000000000036, 0.5773502691896262862, -1.000000000000000000 ) ) ;
#4392=CARTESIAN_POINT ( 'NONE',  ( 9.650000000000000355, 1.665213485140613626E-16, -1.219500000000000028 ) ) ;
#4408=DIRECTION ( 'NONE',  ( -1.000000000000000000, -0.000000000000000000, -0.000000000000000000 ) ) ;
#4433=CARTESIAN_POINT ( 'NONE',  ( 1.649999999999999911, 0.000000000000000000, 0.000000000000000000 ) ) ;
#4478=CIRCLE ( 'NONE', #8862, 3.351416843938787249 ) ;
#4484=ADVANCED_FACE ( 'NONE', ( #562 ), #12553, .T. ) ;
#4497=DIRECTION ( 'NONE',  ( 0.000000000000000000, 0.8660254037844387076, 0.4999999999999998890 ) ) ;
#4505=DIRECTION ( 'NONE',  ( 0.000000000000000000, 0.000000000000000000, 1.000000000000000000 ) ) ;
#4509=ORIENTED_EDGE ( 'NONE', *, *, #976, .F. ) ;
#4519=ORIENTED_EDGE ( 'NONE', *, *, #5879, .F. ) ;
#4531=EDGE_LOOP ( 'NONE', ( #11178, #2768, #627, #12767, #2752 ) ) ;
#4535=LINE ( 'NONE', #9569, #2236 ) ;
#4537=AXIS2_PLACEMENT_3D ( 'NONE', #4101, #11083, #1207 ) ;
#4544=DIRECTION ( 'NONE',  ( 0.000000000000000000, 0.000000000000000000, 1.000000000000000000 ) ) ;
#4548=DIRECTION ( 'NONE',  ( -1.000000000000000000, -0.000000000000000000, -0.000000000000000000 ) ) ;
#4551=DIRECTION ( 'NONE',  ( 0.000000000000000000, 0.000000000000000000, 1.000000000000000000 ) ) ;
#4583=CARTESIAN_POINT ( 'NONE',  ( 1.617350269189632428, 0.000000000000000000, 0.000000000000000000 ) ) ;
#4591=VERTEX_POINT ( 'NONE', #945 ) ;
#4597=SHAPE_REPRESENTATION ( 'socket button head screw_iso_ISO 7380 - M3 x 8 - 8N', ( #5704 ), #11138 ) ;
#4614=EDGE_CURVE ( 'NONE', #10459, #12299, #6199, .T. ) ;
#4619=VECTOR ( 'NONE', #8790, 1000.000000000000114 ) ;
#4667=CARTESIAN_POINT ( 'NONE',  ( 1.749999999999999112, 1.959434878635763504E-16, -1.599999999999998757 ) ) ;
#4669=PLANE ( 'NONE',  #2302 ) ;
#4691=ORIENTED_EDGE ( 'NONE', *, *, #8088, .F. ) ;
#4719=ORIENTED_EDGE ( 'NONE', *, *, #10822, .F. ) ;
#4735=LINE ( 'NONE', #1982, #2615 ) ;
#4750=DIRECTION ( 'NONE',  ( -0.000000000000000000, -0.5000000000000003331, 0.8660254037844384856 ) ) ;
#4772=ADVANCED_FACE ( 'NONE', ( #2136, #215 ), #4359, .F. ) ;
#4776=ORIENTED_EDGE ( 'NONE', *, *, #9631, .F. ) ;
#4781=VERTEX_POINT ( 'NONE', #2337 ) ;
#4805=CARTESIAN_POINT ( 'NONE',  ( 1.040000000000000036, 0.5773502691896262862, 1.000000000000000000 ) ) ;
#4811=EDGE_CURVE ( 'NONE', #9018, #571, #613, .T. ) ;
#4824=DIRECTION ( 'NONE',  ( 0.000000000000000000, 0.000000000000000000, 1.000000000000000000 ) ) ;
#4859=DIRECTION ( 'NONE',  ( 0.000000000000000000, 0.000000000000000000, 1.000000000000000000 ) ) ;
#4886=DIRECTION ( 'NONE',  ( 1.000000000000000000, 0.000000000000000000, 0.000000000000000000 ) ) ;
#4911=VERTEX_POINT ( 'NONE', #3642 ) ;
#4922=PLANE ( 'NONE',  #2076 ) ;
#4924=AXIS2_PLACEMENT_3D ( 'NONE', #8417, #9765, #3389 ) ;
#4930=ADVANCED_FACE ( 'NONE', ( #7494 ), #9560, .F. ) ;
#4946=ORIENTED_EDGE ( 'NONE', *, *, #9012, .F. ) ;
#4994=UNCERTAINTY_MEASURE_WITH_UNIT (LENGTH_MEASURE( 1.000000000000000082E-05 ), #3069, 'distance_accuracy_value', 'NONE');
#5049=DIRECTION ( 'NONE',  ( -0.7071067811865489050, 8.659560562354915602E-17, -0.7071067811865462405 ) ) ;
#5076=VERTEX_POINT ( 'NONE', #1064 ) ;
#5100=DIRECTION ( 'NONE',  ( 0.000000000000000000, -1.000000000000000000, 0.000000000000000000 ) ) ;
#5130=FACE_OUTER_BOUND ( 'NONE', #7453, .T. ) ;
#5138=AXIS2_PLACEMENT_3D ( 'NONE', #3654, #10583, #686 ) ;
#5148=( LENGTH_UNIT ( ) NAMED_UNIT ( * ) SI_UNIT ( .MILLI., .METRE. ) );
#5180=CARTESIAN_POINT ( 'NONE',  ( 1.269999999999999796, -2.850000000000002753, -3.490243377569956061E-16 ) ) ;
#5204=VERTEX_POINT ( 'NONE', #10229 ) ;
#5206=AXIS2_PLACEMENT_3D ( 'NONE', #11523, #2568, #845 ) ;
#5252=DIRECTION ( 'NONE',  ( 0.000000000000000000, -0.8660254037844384856, -0.5000000000000003331 ) ) ;
#5264=DIRECTION ( 'NONE',  ( 0.000000000000000000, 0.000000000000000000, 1.000000000000000000 ) ) ;
#5265=ORIENTED_EDGE ( 'NONE', *, *, #6068, .T. ) ;
#5274=EDGE_CURVE ( 'NONE', #1701, #7344, #3371, .T. ) ;
#5276=PLANE ( 'NONE',  #11390 ) ;
#5286=ORIENTED_EDGE ( 'NONE', *, *, #4123, .F. ) ;
#5297=CARTESIAN_POINT ( 'NONE',  ( 1.040000000000000036, 0.5773502691896262862, -1.000000000000000000 ) ) ;
#5299=( GEOMETRIC_REPRESENTATION_CONTEXT ( 3 ) GLOBAL_UNCERTAINTY_ASSIGNED_CONTEXT ( ( #4994 ) ) GLOBAL_UNIT_ASSIGNED_CONTEXT ( ( #3069, #8100, #12087 ) ) REPRESENTATION_CONTEXT ( 'NONE', 'WORKASPACE' ) );
#5303=CLOSED_SHELL ( 'NONE', ( #2353, #824, #3930, #12816, #1435, #12720, #7027, #8380, #3878, #4772, #11917, #3569, #2002, #4930, #3853, #1787, #1565, #6934, #11155, #12690, #10564, #6160, #125, #6870, #8492, #4484, #6867 ) ) ;
#5305=ORIENTED_EDGE ( 'NONE', *, *, #8626, .T. ) ;
#5324=DIRECTION ( 'NONE',  ( -0.000000000000000000, -0.5000000000000003331, 0.8660254037844384856 ) ) ;
#5332=ORIENTED_EDGE ( 'NONE', *, *, #678, .F. ) ;
#5357=VECTOR ( 'NONE', #6489, 1000.000000000000000 ) ;
#5376=DIRECTION ( 'NONE',  ( -0.000000000000000000, 0.4999999999999998890, -0.8660254037844387076 ) ) ;
#5431=ORIENTED_EDGE ( 'NONE', *, *, #4811, .T. ) ;
#5473=DIRECTION ( 'NONE',  ( 0.000000000000000000, 0.000000000000000000, 1.000000000000000000 ) ) ;
#5496=ORIENTED_EDGE ( 'NONE', *, *, #5971, .F. ) ;
#5507=VECTOR ( 'NONE', #5866, 1000.000000000000000 ) ;
#5520=LINE ( 'NONE', #4805, #4619 ) ;
#5526=VECTOR ( 'NONE', #3823, 1000.000000000000000 ) ;
#5544=CARTESIAN_POINT ( 'NONE',  ( 1.040000000000000036, 0.000000000000000000, 0.000000000000000000 ) ) ;
#5556=AXIS2_PLACEMENT_3D ( 'NONE', #926, #10999, #6888 ) ;
#5614=CIRCLE ( 'NONE', #4366, 1.000000000000000000 ) ;
#5630=CARTESIAN_POINT ( 'NONE',  ( 0.000000000000000000, 0.000000000000000000, 1.499999999999998668 ) ) ;
#5637=ORIENTED_EDGE ( 'NONE', *, *, #12153, .T. ) ;
#5680=LINE ( 'NONE', #8570, #580 ) ;
#5681=ORIENTED_EDGE ( 'NONE', *, *, #8127, .F. ) ;
#5704=AXIS2_PLACEMENT_3D ( 'NONE', #8997, #4824, #4886 ) ;
#5719=ORIENTED_EDGE ( 'NONE', *, *, #12064, .T. ) ;
#5725=DIRECTION ( 'NONE',  ( -1.000000000000000000, 0.000000000000000000, 0.000000000000000000 ) ) ;
#5751=EDGE_CURVE ( 'NONE', #3765, #488, #10603, .T. ) ;
#5757=DIRECTION ( 'NONE',  ( -1.000000000000000000, -0.000000000000000000, -0.000000000000000000 ) ) ;
#5778=CARTESIAN_POINT ( 'NONE',  ( 1.040000000000000036, -0.5773502691896255090, 1.000000000000000000 ) ) ;
#5865=EDGE_CURVE ( 'NONE', #3479, #4781, #7068, .T. ) ;
#5866=DIRECTION ( 'NONE',  ( -0.000000000000000000, -0.4999999999999999445, -0.8660254037844387076 ) ) ;
#5879=EDGE_CURVE ( 'NONE', #3526, #11890, #9015, .T. ) ;
#5895=ORIENTED_EDGE ( 'NONE', *, *, #5865, .T. ) ;
#5932=( NAMED_UNIT ( * ) PLANE_ANGLE_UNIT ( ) SI_UNIT ( $, .RADIAN. ) );
#5952=CARTESIAN_POINT ( 'NONE',  ( 4.336808689942017736E-16, 1.424999999999999600, 0.000000000000000000 ) ) ;
#5970=ORIENTED_EDGE ( 'NONE', *, *, #3165, .F. ) ;
#5971=EDGE_CURVE ( 'NONE', #7840, #4911, #6328, .T. ) ;
#6002=ORIENTED_EDGE ( 'NONE', *, *, #7724, .F. ) ;
#6047=PLANE ( 'NONE',  #4537 ) ;
#6068=EDGE_CURVE ( 'NONE', #571, #8179, #6437, .T. ) ;
#6088=EDGE_CURVE ( 'NONE', #4781, #7005, #7640, .T. ) ;
#6110=CYLINDRICAL_SURFACE ( 'NONE', #540, 2.849999999999999201 ) ;
#6129=PRODUCT_DEFINITION_FORMATION_WITH_SPECIFIED_SOURCE ( 'ANY', '', #1451, .NOT_KNOWN. ) ;
#6132=TOROIDAL_SURFACE ( 'NONE', #713, 1.599999999999998757, 0.1000000000000000056 ) ;
#6134=FACE_OUTER_BOUND ( 'NONE', #10601, .T. ) ;
#6160=ADVANCED_FACE ( 'NONE', ( #3848 ), #3721, .T. ) ;
#6174=CARTESIAN_POINT ( 'NONE',  ( 1.617350269189632428, 0.000000000000000000, 0.000000000000000000 ) ) ;
#6192=DIRECTION ( 'NONE',  ( 1.000000000000000000, 0.000000000000000000, -0.000000000000000000 ) ) ;
#6199=CIRCLE ( 'NONE', #2662, 1.219500000000000028 ) ;
#6224=ORIENTED_EDGE ( 'NONE', *, *, #6068, .F. ) ;
#6234=DIRECTION ( 'NONE',  ( 0.000000000000000000, 0.5000000000000003331, -0.8660254037844384856 ) ) ;
#6274=ORIENTED_EDGE ( 'NONE', *, *, #5865, .F. ) ;
#6295=CARTESIAN_POINT ( 'NONE',  ( 0.000000000000000000, -1.154700538379251240, 1.014316938424154191E-17 ) ) ;
#6306=EDGE_CURVE ( 'NONE', #4911, #571, #5614, .T. ) ;
#6328=LINE ( 'NONE', #8305, #12294 ) ;
#6350=ORIENTED_EDGE ( 'NONE', *, *, #4091, .F. ) ;
#6365=CARTESIAN_POINT ( 'NONE',  ( 1.749999999999999112, 0.000000000000000000, 0.000000000000000000 ) ) ;
#6372=CARTESIAN_POINT ( 'NONE',  ( 1.040000000000000036, 0.000000000000000000, 0.000000000000000000 ) ) ;
#6374=FACE_OUTER_BOUND ( 'NONE', #1119, .T. ) ;
#6390=ORIENTED_EDGE ( 'NONE', *, *, #1049, .T. ) ;
#6418=ORIENTED_EDGE ( 'NONE', *, *, #4062, .T. ) ;
#6436=ORIENTED_EDGE ( 'NONE', *, *, #9753, .T. ) ;
#6437=CIRCLE ( 'NONE', #10207, 1.000000000000000000 ) ;
#6445=CARTESIAN_POINT ( 'NONE',  ( 1.269999999999999796, 0.000000000000000000, 0.000000000000000000 ) ) ;
#6447=ORIENTED_EDGE ( 'NONE', *, *, #9012, .T. ) ;
#6453=CIRCLE ( 'NONE', #8373, 1.499999999999998668 ) ;
#6489=DIRECTION ( 'NONE',  ( -0.000000000000000000, -0.4999999999999999445, -0.8660254037844387076 ) ) ;
#6500=DIRECTION ( 'NONE',  ( -1.000000000000000000, 0.000000000000000000, 0.000000000000000000 ) ) ;
#6531=DIRECTION ( 'NONE',  ( 0.000000000000000000, 0.000000000000000000, 1.000000000000000000 ) ) ;
#6582=FACE_OUTER_BOUND ( 'NONE', #8902, .T. ) ;
#6595=EDGE_CURVE ( 'NONE', #10269, #571, #9222, .T. ) ;
#6641=DIRECTION ( 'NONE',  ( -0.000000000000000000, 0.5000000000000003331, 0.8660254037844384856 ) ) ;
#6644=AXIS2_PLACEMENT_3D ( 'NONE', #6927, #12029, #3142 ) ;
#6651=DIRECTION ( 'NONE',  ( -1.000000000000000000, -0.000000000000000000, -0.000000000000000000 ) ) ;
#6686=DIRECTION ( 'NONE',  ( 0.000000000000000000, -0.5000000000000003331, -0.8660254037844384856 ) ) ;
#6691=LINE ( 'NONE', #859, #12435 ) ;
#6715=CARTESIAN_POINT ( 'NONE',  ( 0.000000000000000000, 0.000000000000000000, 0.000000000000000000 ) ) ;
#6757=EDGE_CURVE ( 'NONE', #488, #1106, #10008, .T. ) ;
#6859=ORIENTED_EDGE ( 'NONE', *, *, #2567, .F. ) ;
#6867=ADVANCED_FACE ( 'NONE', ( #12903 ), #2502, .F. ) ;
#6870=ADVANCED_FACE ( 'NONE', ( #12714 ), #4669, .T. ) ;
#6882=EDGE_LOOP ( 'NONE', ( #8395, #10715, #4003, #5332, #2159 ) ) ;
#6888=DIRECTION ( 'NONE',  ( 0.000000000000000000, 0.000000000000000000, 1.000000000000000000 ) ) ;
#6889=ORIENTED_EDGE ( 'NONE', *, *, #678, .T. ) ;
#6898=CARTESIAN_POINT ( 'NONE',  ( 1.749999999999999112, 0.000000000000000000, 1.499999999999998668 ) ) ;
#6927=CARTESIAN_POINT ( 'NONE',  ( 1.649999999999999911, 0.000000000000000000, 0.000000000000000000 ) ) ;
#6934=ADVANCED_FACE ( 'NONE', ( #12777 ), #4922, .T. ) ;
#6947=DIRECTION ( 'NONE',  ( -1.000000000000000000, -0.000000000000000000, -0.000000000000000000 ) ) ;
#6977=DIRECTION ( 'NONE',  ( -1.000000000000000000, 0.000000000000000000, 0.000000000000000000 ) ) ;
#7005=VERTEX_POINT ( 'NONE', #2247 ) ;
#7027=ADVANCED_FACE ( 'NONE', ( #3161, #8191 ), #9955, .T. ) ;
#7035=CARTESIAN_POINT ( 'NONE',  ( 1.040000000000000036, 0.5773502691896262862, 1.000000000000000000 ) ) ;
#7068=CIRCLE ( 'NONE', #6644, 2.849999999999999201 ) ;
#7109=UNCERTAINTY_MEASURE_WITH_UNIT (LENGTH_MEASURE( 1.000000000000000082E-05 ), #5148, 'distance_accuracy_value', 'NONE');
#7112=CARTESIAN_POINT ( 'NONE',  ( 0.000000000000000000, 0.000000000000000000, 0.000000000000000000 ) ) ;
#7166=DIRECTION ( 'NONE',  ( -1.000000000000000000, 0.000000000000000000, -0.000000000000000000 ) ) ;
#7176=ORIENTED_EDGE ( 'NONE', *, *, #1023, .T. ) ;
#7177=( LENGTH_UNIT ( ) NAMED_UNIT ( * ) SI_UNIT ( .MILLI., .METRE. ) );
#7184=CARTESIAN_POINT ( 'NONE',  ( 3.033375984251971413, -3.035766082959412415E-15, 0.000000000000000000 ) ) ;
#7198=EDGE_CURVE ( 'NONE', #3479, #4591, #5680, .T. ) ;
#7201=CARTESIAN_POINT ( 'NONE',  ( 0.000000000000000000, 0.5773502691896262862, -1.000000000000000000 ) ) ;
#7240=VECTOR ( 'NONE', #10953, 1000.000000000000000 ) ;
#7271=DIRECTION ( 'NONE',  ( -1.000000000000000000, 0.000000000000000000, -0.000000000000000000 ) ) ;
#7282=PLANE ( 'NONE',  #1051 ) ;
#7295=AXIS2_PLACEMENT_3D ( 'NONE', #6365, #10362, #7610 ) ;
#7300=ORIENTED_EDGE ( 'NONE', *, *, #322, .F. ) ;
#7312=CARTESIAN_POINT ( 'NONE',  ( 1.649999999999999911, 3.490243377569955568E-16, -2.849999999999999201 ) ) ;
#7344=VERTEX_POINT ( 'NONE', #9065 ) ;
#7348=CARTESIAN_POINT ( 'NONE',  ( 1.040000000000000036, -0.5773502691896256200, -1.000000000000000000 ) ) ;
#7356=AXIS2_PLACEMENT_3D ( 'NONE', #9372, #4408, #3429 ) ;
#7357=CARTESIAN_POINT ( 'NONE',  ( 9.650000000000000355, 0.000000000000000000, 0.000000000000000000 ) ) ;
#7370=DIRECTION ( 'NONE',  ( 0.000000000000000000, 0.000000000000000000, 1.000000000000000000 ) ) ;
#7382=ORIENTED_EDGE ( 'NONE', *, *, #976, .T. ) ;
#7409=FACE_OUTER_BOUND ( 'NONE', #6882, .T. ) ;
#7451=VERTEX_POINT ( 'NONE', #11088 ) ;
#7453=EDGE_LOOP ( 'NONE', ( #3332, #4035 ) ) ;
#7457=CONICAL_SURFACE ( 'NONE', #1814, 1.219500000000000028, 0.7853981633974463916 ) ;
#7485=CARTESIAN_POINT ( 'NONE',  ( 1.749999999999999112, 0.000000000000000000, 0.000000000000000000 ) ) ;
#7494=FACE_OUTER_BOUND ( 'NONE', #8520, .T. ) ;
#7512=CARTESIAN_POINT ( 'NONE',  ( 1.040000000000000036, 0.5773502691896262862, -1.000000000000000000 ) ) ;
#7539=ORIENTED_EDGE ( 'NONE', *, *, #632, .F. ) ;
#7572=CIRCLE ( 'NONE', #7356, 1.424999999999999822 ) ;
#7603=ORIENTED_EDGE ( 'NONE', *, *, #4062, .F. ) ;
#7606=DIRECTION ( 'NONE',  ( 0.000000000000000000, 0.000000000000000000, 1.000000000000000000 ) ) ;
#7610=DIRECTION ( 'NONE',  ( 0.000000000000000000, 0.000000000000000000, 1.000000000000000000 ) ) ;
#7611=CARTESIAN_POINT ( 'NONE',  ( 1.649999999999999023, 0.000000000000000000, 0.000000000000000000 ) ) ;
#7633=CARTESIAN_POINT ( 'NONE',  ( 1.040000000000000036, -1.154700538379251240, 1.014316938424154191E-17 ) ) ;
#7636=ORIENTED_EDGE ( 'NONE', *, *, #2916, .F. ) ;
#7640=LINE ( 'NONE', #9666, #2485 ) ;
#7661=AXIS2_PLACEMENT_3D ( 'NONE', #2381, #3369, #7606 ) ;
#7687=CARTESIAN_POINT ( 'NONE',  ( 1.749999999999999112, 0.000000000000000000, 0.000000000000000000 ) ) ;
#7690=EDGE_CURVE ( 'NONE', #5204, #12162, #8612, .T. ) ;
#7706=AXIS2_PLACEMENT_3D ( 'NONE', #2676, #3596, #3045 ) ;
#7724=EDGE_CURVE ( 'NONE', #5204, #11636, #8799, .T. ) ;
#7732=CIRCLE ( 'NONE', #9399, 2.849999999999999201 ) ;
#7763=ORIENTED_EDGE ( 'NONE', *, *, #6757, .F. ) ;
#7806=EDGE_CURVE ( 'NONE', #3174, #11441, #4478, .T. ) ;
#7809=ORIENTED_EDGE ( 'NONE', *, *, #12064, .F. ) ;
#7823=CARTESIAN_POINT ( 'NONE',  ( 0.000000000000000000, 0.5773502691896262862, -1.000000000000000000 ) ) ;
#7835=CIRCLE ( 'NONE', #11809, 3.351416843938787249 ) ;
#7840=VERTEX_POINT ( 'NONE', #10884 ) ;
#7871=LINE ( 'NONE', #9959, #5526 ) ;
#7932=DIRECTION ( 'NONE',  ( 0.000000000000000000, 0.000000000000000000, 1.000000000000000000 ) ) ;
#7967=CYLINDRICAL_SURFACE ( 'NONE', #1994, 2.849999999999999201 ) ;
#7970=PRESENTATION_STYLE_ASSIGNMENT (( #3987 ) ) ;
#7983=ORIENTED_EDGE ( 'NONE', *, *, #10637, .T. ) ;
#8013=DIRECTION ( 'NONE',  ( 0.000000000000000000, 0.000000000000000000, 1.000000000000000000 ) ) ;
#8032=EDGE_LOOP ( 'NONE', ( #6002, #10520, #7539 ) ) ;
#8072=DIRECTION ( 'NONE',  ( -1.000000000000000000, -0.000000000000000000, -0.000000000000000000 ) ) ;
#8081=EDGE_CURVE ( 'NONE', #2507, #865, #3460, .T. ) ;
#8088=EDGE_CURVE ( 'NONE', #5076, #9939, #1561, .T. ) ;
#8089=CARTESIAN_POINT ( 'NONE',  ( 1.649999999999999023, 1.499999999999997113, 0.000000000000000000 ) ) ;
#8100=( NAMED_UNIT ( * ) PLANE_ANGLE_UNIT ( ) SI_UNIT ( $, .RADIAN. ) );
#8110=ORIENTED_EDGE ( 'NONE', *, *, #12070, .F. ) ;
#8127=EDGE_CURVE ( 'NONE', #1488, #11890, #4735, .T. ) ;
#8135=LINE ( 'NONE', #4338, #11562 ) ;
#8168=CARTESIAN_POINT ( 'NONE',  ( 9.650000000000000355, 0.000000000000000000, 0.000000000000000000 ) ) ;
#8179=VERTEX_POINT ( 'NONE', #10684 ) ;
#8191=FACE_BOUND ( 'NONE', #11129, .T. ) ;
#8259=ORIENTED_EDGE ( 'NONE', *, *, #7690, .T. ) ;
#8300=EDGE_LOOP ( 'NONE', ( #135, #3623, #3659, #8743, #12692 ) ) ;
#8302=ORIENTED_EDGE ( 'NONE', *, *, #4091, .T. ) ;
#8305=CARTESIAN_POINT ( 'NONE',  ( 1.040000000000000036, 1.154700538379252350, 7.017607234860990640E-28 ) ) ;
#8334=LINE ( 'NONE', #6295, #5357 ) ;
#8342=LINE ( 'NONE', #2130, #9489 ) ;
#8344=DIRECTION ( 'NONE',  ( -1.000000000000000000, 0.000000000000000000, -0.000000000000000000 ) ) ;
#8365=DIRECTION ( 'NONE',  ( 0.000000000000000000, 0.000000000000000000, 1.000000000000000000 ) ) ;
#8373=AXIS2_PLACEMENT_3D ( 'NONE', #7485, #468, #2651 ) ;
#8380=ADVANCED_FACE ( 'NONE', ( #8771 ), #9814, .T. ) ;
#8395=ORIENTED_EDGE ( 'NONE', *, *, #7724, .T. ) ;
#8417=CARTESIAN_POINT ( 'NONE',  ( 1.040000000000000036, 0.000000000000000000, 0.000000000000000000 ) ) ;
#8426=ORIENTED_EDGE ( 'NONE', *, *, #7806, .F. ) ;
#8454=ORIENTED_EDGE ( 'NONE', *, *, #1233, .F. ) ;
#8475=DIRECTION ( 'NONE',  ( 0.000000000000000000, 0.000000000000000000, 1.000000000000000000 ) ) ;
#8492=ADVANCED_FACE ( 'NONE', ( #6134 ), #10979, .T. ) ;
#8520=EDGE_LOOP ( 'NONE', ( #8921, #4946, #2285, #1970 ) ) ;
#8566=DIRECTION ( 'NONE',  ( -1.000000000000000000, -0.000000000000000000, -0.000000000000000000 ) ) ;
#8570=CARTESIAN_POINT ( 'NONE',  ( 0.000000000000000000, 3.490243377569955568E-16, -2.849999999999999201 ) ) ;
#8578=ORIENTED_EDGE ( 'NONE', *, *, #97, .T. ) ;
#8605=VECTOR ( 'NONE', #2434, 1000.000000000000114 ) ;
#8612=LINE ( 'NONE', #3646, #2607 ) ;
#8626=EDGE_CURVE ( 'NONE', #9403, #7451, #7835, .T. ) ;
#8659=DIRECTION ( 'NONE',  ( -1.000000000000000000, 0.000000000000000000, 0.000000000000000000 ) ) ;
#8693=ORIENTED_EDGE ( 'NONE', *, *, #6306, .F. ) ;
#8743=ORIENTED_EDGE ( 'NONE', *, *, #632, .T. ) ;
#8753=CARTESIAN_POINT ( 'NONE',  ( 1.040000000000000036, -1.154700538379251240, 1.014316938424154191E-17 ) ) ;
#8771=FACE_OUTER_BOUND ( 'NONE', #10694, .T. ) ;
#8788=DIRECTION ( 'NONE',  ( -0.000000000000000000, 0.4999999999999998890, -0.8660254037844387076 ) ) ;
#8790=DIRECTION ( 'NONE',  ( -0.000000000000000000, -0.5000000000000003331, 0.8660254037844384856 ) ) ;
#8799=LINE ( 'NONE', #10947, #11154 ) ;
#8818=CARTESIAN_POINT ( 'NONE',  ( 1.040000000000000036, 0.000000000000000000, 1.000000000000000000 ) ) ;
#8828=AXIS2_PLACEMENT_3D ( 'NONE', #6715, #8566, #4505 ) ;
#8829=ORIENTED_EDGE ( 'NONE', *, *, #5751, .F. ) ;
#8862=AXIS2_PLACEMENT_3D ( 'NONE', #12732, #8013, #12791 ) ;
#8871=AXIS2_PLACEMENT_3D ( 'NONE', #8972, #1916, #10872 ) ;
#8878=CARTESIAN_POINT ( 'NONE',  ( 1.040000000000000036, 0.000000000000000000, 2.000000000000000000 ) ) ;
#8891=VECTOR ( 'NONE', #10720, 1000.000000000000114 ) ;
#8902=EDGE_LOOP ( 'NONE', ( #6859, #11244, #2154, #8454 ) ) ;
#8907=CARTESIAN_POINT ( 'NONE',  ( 1.040000000000000036, 1.154700538379252350, 7.017607234860990640E-28 ) ) ;
#8918=AXIS2_PLACEMENT_3D ( 'NONE', #3465, #2738, #5473 ) ;
#8919=DIRECTION ( 'NONE',  ( 0.000000000000000000, 0.000000000000000000, 1.000000000000000000 ) ) ;
#8921=ORIENTED_EDGE ( 'NONE', *, *, #12153, .F. ) ;
#8972=CARTESIAN_POINT ( 'NONE',  ( 1.040000000000000036, 0.000000000000000000, 0.000000000000000000 ) ) ;
#8997=CARTESIAN_POINT ( 'NONE',  ( 0.000000000000000000, 0.000000000000000000, 0.000000000000000000 ) ) ;
#9003=DIRECTION ( 'NONE',  ( 0.000000000000000000, 0.000000000000000000, 1.000000000000000000 ) ) ;
#9012=EDGE_CURVE ( 'NONE', #865, #2507, #1044, .T. ) ;
#9015=LINE ( 'NONE', #38, #9785 ) ;
#9018=VERTEX_POINT ( 'NONE', #6174 ) ;
#9033=CARTESIAN_POINT ( 'NONE',  ( 2.168404344971008868E-16, 0.000000000000000000, 0.000000000000000000 ) ) ;
#9048=DIRECTION ( 'NONE',  ( 0.000000000000000000, 0.000000000000000000, 1.000000000000000000 ) ) ;
#9065=CARTESIAN_POINT ( 'NONE',  ( 0.000000000000000000, -0.5773502691896256200, -1.000000000000000000 ) ) ;
#9067=LINE ( 'NONE', #11225, #9477 ) ;
#9068=ORIENTED_EDGE ( 'NONE', *, *, #12870, .F. ) ;
#9131=EDGE_CURVE ( 'NONE', #1106, #488, #6453, .T. ) ;
#9143=DIRECTION ( 'NONE',  ( -0.000000000000000000, -1.000000000000000000, -0.000000000000000000 ) ) ;
#9209=CARTESIAN_POINT ( 'NONE',  ( 1.040000000000000036, -0.5773502691896255090, 1.000000000000000000 ) ) ;
#9222=LINE ( 'NONE', #5297, #9794 ) ;
#9239=CIRCLE ( 'NONE', #11319, 0.1000000000000000472 ) ;
#9276=SPHERICAL_SURFACE ( 'NONE', #11963, 3.351416843938787249 ) ;
#9290=DIRECTION ( 'NONE',  ( -0.000000000000000000, 1.000000000000000000, -0.000000000000000000 ) ) ;
#9304=EDGE_LOOP ( 'NONE', ( #10315, #7809, #6224 ) ) ;
#9310=LINE ( 'NONE', #7348, #9661 ) ;
#9325=EDGE_LOOP ( 'NONE', ( #1076, #11369, #3809, #132, #12105 ) ) ;
#9346=ORIENTED_EDGE ( 'NONE', *, *, #464, .T. ) ;
#9347=AXIS2_PLACEMENT_3D ( 'NONE', #8089, #7166, #1142 ) ;
#9372=CARTESIAN_POINT ( 'NONE',  ( 4.336808689942017736E-16, 0.000000000000000000, 0.000000000000000000 ) ) ;
#9399=AXIS2_PLACEMENT_3D ( 'NONE', #4433, #3330, #12546 ) ;
#9403=VERTEX_POINT ( 'NONE', #5180 ) ;
#9419=CIRCLE ( 'NONE', #10040, 1.424999999999999822 ) ;
#9428=CIRCLE ( 'NONE', #10682, 0.1000000000000000472 ) ;
#9477=VECTOR ( 'NONE', #2341, 1000.000000000000000 ) ;
#9489=VECTOR ( 'NONE', #5324, 1000.000000000000114 ) ;
#9560=TOROIDAL_SURFACE ( 'NONE', #350, 1.599999999999998757, 0.1000000000000000056 ) ;
#9569=CARTESIAN_POINT ( 'NONE',  ( 1.040000000000000036, -0.5773502691896255090, 1.000000000000000000 ) ) ;
#9575=VECTOR ( 'NONE', #1391, 1000.000000000000000 ) ;
#9582=ORIENTED_EDGE ( 'NONE', *, *, #4123, .T. ) ;
#9594=FACE_OUTER_BOUND ( 'NONE', #1546, .T. ) ;
#9631=EDGE_CURVE ( 'NONE', #3765, #11967, #12538, .T. ) ;
#9661=VECTOR ( 'NONE', #5376, 1000.000000000000000 ) ;
#9666=CARTESIAN_POINT ( 'NONE',  ( 0.000000000000000000, 0.000000000000000000, 2.849999999999999201 ) ) ;
#9698=EDGE_CURVE ( 'NONE', #3174, #4591, #12319, .T. ) ;
#9722=CARTESIAN_POINT ( 'NONE',  ( 9.369499999999998607, 0.000000000000000000, 1.500000000000000222 ) ) ;
#9733=CARTESIAN_POINT ( 'NONE',  ( 1.040000000000000036, 0.5773502691896262862, 1.000000000000000000 ) ) ;
#9753=EDGE_CURVE ( 'NONE', #7005, #3174, #11482, .T. ) ;
#9754=DIRECTION ( 'NONE',  ( 0.000000000000000000, 0.000000000000000000, 1.000000000000000000 ) ) ;
#9764=CARTESIAN_POINT ( 'NONE',  ( 1.040000000000000036, 0.000000000000000000, 2.000000000000000000 ) ) ;
#9765=DIRECTION ( 'NONE',  ( -1.000000000000000000, -0.000000000000000000, -0.000000000000000000 ) ) ;
#9785=VECTOR ( 'NONE', #9143, 1000.000000000000000 ) ;
#9791=EDGE_LOOP ( 'NONE', ( #4509, #773, #11643, #2275 ) ) ;
#9794=VECTOR ( 'NONE', #9290, 1000.000000000000000 ) ;
#9799=ORIENTED_EDGE ( 'NONE', *, *, #12163, .F. ) ;
#9807=AXIS2_PLACEMENT_3D ( 'NONE', #854, #10683, #4859 ) ;
#9814=SPHERICAL_SURFACE ( 'NONE', #1996, 3.351416843938787249 ) ;
#9816=DIRECTION ( 'NONE',  ( -1.000000000000000000, -0.000000000000000000, -0.000000000000000000 ) ) ;
#9831=DIRECTION ( 'NONE',  ( -0.000000000000000000, -1.000000000000000000, -0.000000000000000000 ) ) ;
#9854=PRODUCT_DEFINITION ( 'UNKNOWN', '', #6129, #10393 ) ;
#9919=VECTOR ( 'NONE', #6641, 1000.000000000000114 ) ;
#9923=FACE_OUTER_BOUND ( 'NONE', #9325, .T. ) ;
#9935=CIRCLE ( 'NONE', #4924, 1.000000000000000000 ) ;
#9939=VERTEX_POINT ( 'NONE', #8818 ) ;
#9940=EDGE_LOOP ( 'NONE', ( #4189, #771 ) ) ;
#9943=VECTOR ( 'NONE', #11862, 1000.000000000000000 ) ;
#9944=DIRECTION ( 'NONE',  ( -1.000000000000000000, -0.000000000000000000, -0.000000000000000000 ) ) ;
#9955=PLANE ( 'NONE',  #11269 ) ;
#9959=CARTESIAN_POINT ( 'NONE',  ( 0.000000000000000000, 1.836970198721028208E-16, -1.499999999999998668 ) ) ;
#10002=ORIENTED_EDGE ( 'NONE', *, *, #7198, .F. ) ;
#10008=CIRCLE ( 'NONE', #7295, 1.499999999999998668 ) ;
#10040=AXIS2_PLACEMENT_3D ( 'NONE', #2973, #8072, #8919 ) ;
#10074=DIRECTION ( 'NONE',  ( -0.7071067811865489050, 0.000000000000000000, 0.7071067811865462405 ) ) ;
#10081=CARTESIAN_POINT ( 'NONE',  ( 1.749999999999999112, 1.836970198721028208E-16, -1.499999999999998668 ) ) ;
#10104=DIRECTION ( 'NONE',  ( -1.000000000000000000, -0.000000000000000000, -0.000000000000000000 ) ) ;
#10117=AXIS2_PLACEMENT_3D ( 'NONE', #7611, #6947, #10744 ) ;
#10188=DIRECTION ( 'NONE',  ( -1.000000000000000000, -0.000000000000000000, -0.000000000000000000 ) ) ;
#10207=AXIS2_PLACEMENT_3D ( 'NONE', #5544, #1749, #3662 ) ;
#10223=ORIENTED_EDGE ( 'NONE', *, *, #1049, .F. ) ;
#10227=EDGE_CURVE ( 'NONE', #4781, #3479, #7732, .T. ) ;
#10229=CARTESIAN_POINT ( 'NONE',  ( 1.040000000000000036, 1.154700538379252350, 7.017607234860990640E-28 ) ) ;
#10230=DIRECTION ( 'NONE',  ( -1.000000000000000000, -0.000000000000000000, -0.000000000000000000 ) ) ;
#10269=VERTEX_POINT ( 'NONE', #12673 ) ;
#10287=CARTESIAN_POINT ( 'NONE',  ( 1.040000000000000036, 0.5773502691896262862, 1.000000000000000000 ) ) ;
#10315=ORIENTED_EDGE ( 'NONE', *, *, #6595, .F. ) ;
#10330=DIRECTION ( 'NONE',  ( 0.000000000000000000, 1.224646799147353207E-16, -1.000000000000000000 ) ) ;
#10334=PRODUCT_CONTEXT ( 'NONE', #4174, 'mechanical' ) ;
#10337=EDGE_CURVE ( 'NONE', #5076, #58, #10768, .T. ) ;
#10360=CARTESIAN_POINT ( 'NONE',  ( 1.040000000000000036, 0.000000000000000000, 0.000000000000000000 ) ) ;
#10362=DIRECTION ( 'NONE',  ( 1.000000000000000000, 0.000000000000000000, 0.000000000000000000 ) ) ;
#10393=PRODUCT_DEFINITION_CONTEXT ( 'detailed design', #1590, 'design' ) ;
#10444=VERTEX_POINT ( 'NONE', #7035 ) ;
#10459=VERTEX_POINT ( 'NONE', #12926 ) ;
#10506=ORIENTED_EDGE ( 'NONE', *, *, #8081, .T. ) ;
#10508=DIRECTION ( 'NONE',  ( 0.000000000000000000, -0.4999999999999998890, 0.8660254037844387076 ) ) ;
#10520=ORIENTED_EDGE ( 'NONE', *, *, #1803, .F. ) ;
#10521=COLOUR_RGB ( '',1.000000000000000000, 0.9490196078431372140, 0.9098039215686274384 ) ;
#10524=CARTESIAN_POINT ( 'NONE',  ( 3.033375984251971413, -3.035766082959412415E-15, 0.000000000000000000 ) ) ;
#10554=DIRECTION ( 'NONE',  ( -0.000000000000000000, 1.000000000000000000, 1.224646799147353207E-16 ) ) ;
#10564=ADVANCED_FACE ( 'NONE', ( #82 ), #12139, .T. ) ;
#10583=DIRECTION ( 'NONE',  ( -1.000000000000000000, -0.000000000000000000, -0.000000000000000000 ) ) ;
#10601=EDGE_LOOP ( 'NONE', ( #10223, #2034, #95 ) ) ;
#10603=LINE ( 'NONE', #5630, #11456 ) ;
#10636=LINE ( 'NONE', #2667, #9919 ) ;
#10637=EDGE_CURVE ( 'NONE', #8179, #5076, #2734, .T. ) ;
#10682=AXIS2_PLACEMENT_3D ( 'NONE', #12830, #5100, #50 ) ;
#10683=DIRECTION ( 'NONE',  ( -1.000000000000000000, -0.000000000000000000, -0.000000000000000000 ) ) ;
#10684=CARTESIAN_POINT ( 'NONE',  ( 1.040000000000000036, -0.8660254037844385966, -0.4999999999999997780 ) ) ;
#10694=EDGE_LOOP ( 'NONE', ( #1091, #9346, #6436, #11972, #246 ) ) ;
#10715=ORIENTED_EDGE ( 'NONE', *, *, #10822, .T. ) ;
#10720=DIRECTION ( 'NONE',  ( -0.5000000000000042188, 0.000000000000000000, 0.8660254037844361541 ) ) ;
#10729=EDGE_CURVE ( 'NONE', #58, #1701, #2393, .T. ) ;
#10744=DIRECTION ( 'NONE',  ( 0.000000000000000000, 0.000000000000000000, 1.000000000000000000 ) ) ;
#10768=LINE ( 'NONE', #7633, #2104 ) ;
#10809=CARTESIAN_POINT ( 'NONE',  ( 1.269999999999999796, 2.849999999999999201, 0.000000000000000000 ) ) ;
#10822=EDGE_CURVE ( 'NONE', #11636, #10444, #5520, .T. ) ;
#10872=DIRECTION ( 'NONE',  ( 0.000000000000000000, 0.000000000000000000, 1.000000000000000000 ) ) ;
#10884=CARTESIAN_POINT ( 'NONE',  ( 1.040000000000000036, 0.5773502691896262862, -1.000000000000000000 ) ) ;
#10901=EDGE_LOOP ( 'NONE', ( #8302, #7176, #2975, #4519, #7636 ) ) ;
#10941=EDGE_CURVE ( 'NONE', #7451, #11441, #9419, .T. ) ;
#10947=CARTESIAN_POINT ( 'NONE',  ( 1.040000000000000036, 0.5773502691896262862, 1.000000000000000000 ) ) ;
#10953=DIRECTION ( 'NONE',  ( -0.000000000000000000, 1.000000000000000000, -0.000000000000000000 ) ) ;
#10965=ORIENTED_EDGE ( 'NONE', *, *, #3285, .F. ) ;
#10979=PLANE ( 'NONE',  #12018 ) ;
#10999=DIRECTION ( 'NONE',  ( -1.000000000000000000, -0.000000000000000000, -0.000000000000000000 ) ) ;
#11030=CARTESIAN_POINT ( 'NONE',  ( 1.040000000000000036, -0.5773502691896255090, 1.000000000000000000 ) ) ;
#11044=ORIENTED_EDGE ( 'NONE', *, *, #2567, .T. ) ;
#11083=DIRECTION ( 'NONE',  ( 0.000000000000000000, 0.8660254037844387076, -0.4999999999999998890 ) ) ;
#11088=CARTESIAN_POINT ( 'NONE',  ( 4.336808689942017736E-16, -1.424999999999999822, -2.617682533177465074E-16 ) ) ;
#11099=CARTESIAN_POINT ( 'NONE',  ( 0.000000000000000000, 0.000000000000000000, 0.000000000000000000 ) ) ;
#11103=FACE_OUTER_BOUND ( 'NONE', #11808, .T. ) ;
#11116=LINE ( 'NONE', #12368, #8605 ) ;
#11118=AXIS2_PLACEMENT_3D ( 'NONE', #9209, #1355, #2228 ) ;
#11129=EDGE_LOOP ( 'NONE', ( #12823, #6418, #12801, #11295, #12498, #6889 ) ) ;
#11138=( GEOMETRIC_REPRESENTATION_CONTEXT ( 3 ) GLOBAL_UNCERTAINTY_ASSIGNED_CONTEXT ( ( #3037 ) ) GLOBAL_UNIT_ASSIGNED_CONTEXT ( ( #7177, #5932, #228 ) ) REPRESENTATION_CONTEXT ( 'NONE', 'WORKASPACE' ) );
#11146=CARTESIAN_POINT ( 'NONE',  ( 1.040000000000000036, 0.000000000000000000, 2.000000000000000000 ) ) ;
#11154=VECTOR ( 'NONE', #4750, 1000.000000000000114 ) ;
#11155=ADVANCED_FACE ( 'NONE', ( #7409 ), #7282, .T. ) ;
#11171=FACE_OUTER_BOUND ( 'NONE', #10901, .T. ) ;
#11178=ORIENTED_EDGE ( 'NONE', *, *, #6595, .T. ) ;
#11225=CARTESIAN_POINT ( 'NONE',  ( 1.040000000000000036, 0.5773502691896262862, -1.000000000000000000 ) ) ;
#11235=ORIENTED_EDGE ( 'NONE', *, *, #11434, .F. ) ;
#11237=PLANE ( 'NONE',  #11118 ) ;
#11243=DIRECTION ( 'NONE',  ( -1.000000000000000000, 0.000000000000000000, 0.000000000000000000 ) ) ;
#11244=ORIENTED_EDGE ( 'NONE', *, *, #3494, .T. ) ;
#11264=PRODUCT_DEFINITION_SHAPE ( 'NONE', 'NONE',  #9854 ) ;
#11269=AXIS2_PLACEMENT_3D ( 'NONE', #9033, #7271, #983 ) ;
#11295=ORIENTED_EDGE ( 'NONE', *, *, #3724, .T. ) ;
#11319=AXIS2_PLACEMENT_3D ( 'NONE', #4667, #10554, #1588 ) ;
#11325=ORIENTED_EDGE ( 'NONE', *, *, #6088, .T. ) ;
#11369=ORIENTED_EDGE ( 'NONE', *, *, #7198, .T. ) ;
#11390=AXIS2_PLACEMENT_3D ( 'NONE', #4368, #7370, #6192 ) ;
#11434=EDGE_CURVE ( 'NONE', #865, #488, #9428, .T. ) ;
#11441=VERTEX_POINT ( 'NONE', #5952 ) ;
#11443=LINE ( 'NONE', #4583, #8891 ) ;
#11456=VECTOR ( 'NONE', #5757, 1000.000000000000000 ) ;
#11477=CARTESIAN_POINT ( 'NONE',  ( 2.168404344971008868E-16, -0.5773502691896255090, 1.000000000000000000 ) ) ;
#11478=DIRECTION ( 'NONE',  ( -0.5000000000000042188, 1.060575238724903710E-16, -0.8660254037844361541 ) ) ;
#11482=CIRCLE ( 'NONE', #186, 2.849999999999999201 ) ;
#11495=DIRECTION ( 'NONE',  ( -0.000000000000000000, 1.000000000000000000, -0.000000000000000000 ) ) ;
#11523=CARTESIAN_POINT ( 'NONE',  ( 9.369499999999998607, 0.000000000000000000, 0.000000000000000000 ) ) ;
#11562=VECTOR ( 'NONE', #5049, 1000.000000000000000 ) ;
#11587=VERTEX_POINT ( 'NONE', #7201 ) ;
#11623=DIRECTION ( 'NONE',  ( -0.000000000000000000, -0.4999999999999999445, -0.8660254037844387076 ) ) ;
#11636=VERTEX_POINT ( 'NONE', #1375 ) ;
#11643=ORIENTED_EDGE ( 'NONE', *, *, #5751, .T. ) ;
#11682=CARTESIAN_POINT ( 'NONE',  ( 1.040000000000000036, -0.5773502691896256200, -1.000000000000000000 ) ) ;
#11689=CYLINDRICAL_SURFACE ( 'NONE', #8828, 1.499999999999998668 ) ;
#11705=EDGE_CURVE ( 'NONE', #11587, #12162, #11116, .T. ) ;
#11776=CARTESIAN_POINT ( 'NONE',  ( 3.033375984251971413, -3.035766082959412415E-15, 0.000000000000000000 ) ) ;
#11808=EDGE_LOOP ( 'NONE', ( #2090, #9582, #5305, #8110, #8426 ) ) ;
#11809=AXIS2_PLACEMENT_3D ( 'NONE', #10524, #10330, #12359 ) ;
#11862=DIRECTION ( 'NONE',  ( -1.000000000000000000, 0.000000000000000000, 0.000000000000000000 ) ) ;
#11874=CARTESIAN_POINT ( 'NONE',  ( 1.040000000000000036, 0.000000000000000000, 0.000000000000000000 ) ) ;
#11890=VERTEX_POINT ( 'NONE', #11477 ) ;
#11906=CARTESIAN_POINT ( 'NONE',  ( 1.269999999999999796, 0.000000000000000000, 0.000000000000000000 ) ) ;
#11917=ADVANCED_FACE ( 'NONE', ( #3576 ), #4182, .T. ) ;
#11926=CARTESIAN_POINT ( 'NONE',  ( 1.040000000000000036, -0.5773502691896256200, -1.000000000000000000 ) ) ;
#11963=AXIS2_PLACEMENT_3D ( 'NONE', #7184, #4185, #3277 ) ;
#11967=VERTEX_POINT ( 'NONE', #1533 ) ;
#11972=ORIENTED_EDGE ( 'NONE', *, *, #7806, .T. ) ;
#11998=CIRCLE ( 'NONE', #12420, 1.000000000000000000 ) ;
#12018=AXIS2_PLACEMENT_3D ( 'NONE', #1098, #11243, #12035 ) ;
#12029=DIRECTION ( 'NONE',  ( -1.000000000000000000, -0.000000000000000000, -0.000000000000000000 ) ) ;
#12035=DIRECTION ( 'NONE',  ( 0.000000000000000000, 0.000000000000000000, 1.000000000000000000 ) ) ;
#12037=SHAPE_DEFINITION_REPRESENTATION ( #11264, #4597 ) ;
#12064=EDGE_CURVE ( 'NONE', #8179, #10269, #9310, .T. ) ;
#12070=EDGE_CURVE ( 'NONE', #11441, #7451, #7572, .T. ) ;
#12087=( NAMED_UNIT ( * ) SI_UNIT ( $, .STERADIAN. ) SOLID_ANGLE_UNIT ( ) );
#12105=ORIENTED_EDGE ( 'NONE', *, *, #6088, .F. ) ;
#12109=CARTESIAN_POINT ( 'NONE',  ( 9.650000000000000355, 0.000000000000000000, 1.219500000000000028 ) ) ;
#12116=EDGE_LOOP ( 'NONE', ( #6447, #10506 ) ) ;
#12139=PLANE ( 'NONE',  #4198 ) ;
#12153=EDGE_CURVE ( 'NONE', #2507, #1106, #9239, .T. ) ;
#12162=VERTEX_POINT ( 'NONE', #4072 ) ;
#12163=EDGE_CURVE ( 'NONE', #10459, #3765, #2708, .T. ) ;
#12194=STYLED_ITEM ( 'NONE', ( #7970 ), #1374 ) ;
#12199=DIRECTION ( 'NONE',  ( -1.000000000000000000, -0.000000000000000000, -0.000000000000000000 ) ) ;
#12208=CIRCLE ( 'NONE', #3450, 2.849999999999999201 ) ;
#12265=DIRECTION ( 'NONE',  ( 0.000000000000000000, 0.000000000000000000, 1.000000000000000000 ) ) ;
#12274=ORIENTED_EDGE ( 'NONE', *, *, #5274, .F. ) ;
#12285=SHAPE_REPRESENTATION_RELATIONSHIP ( 'NONE' , 'NONE' ,  #4597, #1374 ) ;
#12294=VECTOR ( 'NONE', #1295, 1000.000000000000114 ) ;
#12299=VERTEX_POINT ( 'NONE', #4392 ) ;
#12319=CIRCLE ( 'NONE', #2717, 2.849999999999999201 ) ;
#12356=ORIENTED_EDGE ( 'NONE', *, *, #10227, .F. ) ;
#12359=DIRECTION ( 'NONE',  ( 0.000000000000000000, 1.000000000000000000, 1.224646799147353207E-16 ) ) ;
#12368=CARTESIAN_POINT ( 'NONE',  ( 0.000000000000000000, 1.154700538379252350, 7.017607234860990640E-28 ) ) ;
#12398=DIRECTION ( 'NONE',  ( -1.000000000000000000, -0.000000000000000000, -0.000000000000000000 ) ) ;
#12403=DIRECTION ( 'NONE',  ( -1.000000000000000000, -0.000000000000000000, -0.000000000000000000 ) ) ;
#12420=AXIS2_PLACEMENT_3D ( 'NONE', #11874, #12858, #12792 ) ;
#12430=EDGE_LOOP ( 'NONE', ( #10002, #5895, #11325, #3273, #5286 ) ) ;
#12435=VECTOR ( 'NONE', #8788, 1000.000000000000000 ) ;
#12460=DIRECTION ( 'NONE',  ( -1.000000000000000000, -0.000000000000000000, -0.000000000000000000 ) ) ;
#12498=ORIENTED_EDGE ( 'NONE', *, *, #11705, .T. ) ;
#12538=CIRCLE ( 'NONE', #5206, 1.500000000000000222 ) ;
#12544=ORIENTED_EDGE ( 'NONE', *, *, #1803, .T. ) ;
#12546=DIRECTION ( 'NONE',  ( 0.000000000000000000, 0.000000000000000000, 1.000000000000000000 ) ) ;
#12551=( NAMED_UNIT ( * ) PLANE_ANGLE_UNIT ( ) SI_UNIT ( $, .RADIAN. ) );
#12553=PLANE ( 'NONE',  #8918 ) ;
#12592=CARTESIAN_POINT ( 'NONE',  ( 1.649999999999999023, 0.000000000000000000, 1.599999999999998757 ) ) ;
#12595=DIRECTION ( 'NONE',  ( 0.000000000000000000, 0.000000000000000000, 1.000000000000000000 ) ) ;
#12625=AXIS2_PLACEMENT_3D ( 'NONE', #8878, #6977, #3919 ) ;
#12632=EDGE_LOOP ( 'NONE', ( #12742, #7382, #4060, #8829 ) ) ;
#12673=CARTESIAN_POINT ( 'NONE',  ( 1.040000000000000036, -0.5773502691896256200, -1.000000000000000000 ) ) ;
#12690=ADVANCED_FACE ( 'NONE', ( #11171 ), #11237, .T. ) ;
#12692=ORIENTED_EDGE ( 'NONE', *, *, #6306, .T. ) ;
#12714=FACE_OUTER_BOUND ( 'NONE', #9304, .T. ) ;
#12720=ADVANCED_FACE ( 'NONE', ( #11103 ), #9276, .T. ) ;
#12732=CARTESIAN_POINT ( 'NONE',  ( 3.033375984251971413, -3.035766082959412415E-15, 0.000000000000000000 ) ) ;
#12742=ORIENTED_EDGE ( 'NONE', *, *, #9631, .T. ) ;
#12744=DIRECTION ( 'NONE',  ( -1.000000000000000000, -0.000000000000000000, -0.000000000000000000 ) ) ;
#12764=DIRECTION ( 'NONE',  ( 0.000000000000000000, 0.000000000000000000, -1.000000000000000000 ) ) ;
#12767=ORIENTED_EDGE ( 'NONE', *, *, #3724, .F. ) ;
#12777=FACE_OUTER_BOUND ( 'NONE', #4084, .T. ) ;
#12783=AXIS2_PLACEMENT_3D ( 'NONE', #11099, #2527, #4551 ) ;
#12791=DIRECTION ( 'NONE',  ( 1.000000000000000000, 0.000000000000000000, 0.000000000000000000 ) ) ;
#12792=DIRECTION ( 'NONE',  ( 0.000000000000000000, 0.000000000000000000, 1.000000000000000000 ) ) ;
#12801=ORIENTED_EDGE ( 'NONE', *, *, #5274, .T. ) ;
#12804=DIRECTION ( 'NONE',  ( -1.000000000000000000, 0.000000000000000000, 0.000000000000000000 ) ) ;
#12816=ADVANCED_FACE ( 'NONE', ( #2675 ), #11689, .T. ) ;
#12818=MECHANICAL_DESIGN_GEOMETRIC_PRESENTATION_REPRESENTATION('',(#12194),#5299);
#12823=ORIENTED_EDGE ( 'NONE', *, *, #5879, .T. ) ;
#12824=DIRECTION ( 'NONE',  ( 0.000000000000000000, 0.000000000000000000, 1.000000000000000000 ) ) ;
#12830=CARTESIAN_POINT ( 'NONE',  ( 1.749999999999999112, 0.000000000000000000, 1.599999999999998757 ) ) ;
#12858=DIRECTION ( 'NONE',  ( -1.000000000000000000, -0.000000000000000000, -0.000000000000000000 ) ) ;
#12865=ORIENTED_EDGE ( 'NONE', *, *, #11705, .F. ) ;
#12870=EDGE_CURVE ( 'NONE', #571, #7840, #1490, .T. ) ;
#12871=MECHANICAL_DESIGN_GEOMETRIC_PRESENTATION_REPRESENTATION('',(#2860),#324);
#12891=DIRECTION ( 'NONE',  ( 0.000000000000000000, 1.000000000000000000, 0.000000000000000000 ) ) ;
#12903=FACE_OUTER_BOUND ( 'NONE', #8300, .T. ) ;
#12926=CARTESIAN_POINT ( 'NONE',  ( 9.650000000000000355, 0.000000000000000000, 1.219500000000000028 ) ) ;
#12936=LINE ( 'NONE', #8753, #5507 ) ;
#12943=FILL_AREA_STYLE ('',( #960 ) ) ;
#12953=ORIENTED_EDGE ( 'NONE', *, *, #1023, .F. ) ;
#13003=COLOUR_RGB('Black',0.12,0.14,0.17);
#13004=FILL_AREA_STYLE_COLOUR('',#13003);
#13005=FILL_AREA_STYLE('',(#13004));
#13006=SURFACE_STYLE_FILL_AREA(#13005);
#13007=SURFACE_SIDE_STYLE('',(#13006));
#13008=SURFACE_STYLE_USAGE(.BOTH.,#13007);
#13009=PRESENTATION_STYLE_ASSIGNMENT((#13008));
ENDSEC;
END-ISO-10303-21;
